ISO-10303-21;
HEADER;
FILE_DESCRIPTION (('STEP AP214'),
    '1' );
FILE_NAME ('socket button head screw_iso_ISO 7380 - M4 x 12 - 12N.step',
    '2026-10-25T16:39:07',
    ( '' ),
    ( '' ),
    'SwSTEP 2.0',
    'SolidWorks 2026',
    '' );
FILE_SCHEMA (( 'AUTOMOTIVE_DESIGN' ));
ENDSEC;

DATA;
#20=AXIS2_PLACEMENT_3D ( 'NONE', #7890, #15986, #13371 ) ;
#81=CARTESIAN_POINT ( 'NONE',  ( 3.885274725274725949, -4.336808689942017736E-16, 0.000000000000000000 ) ) ;
#86=LINE ( 'NONE', #7211, #12515 ) ;
#91=AXIS2_PLACEMENT_3D ( 'NONE', #15450, #198, #8713 ) ;
#115=CARTESIAN_POINT ( 'NONE',  ( 1.300000000000000044, -1.443375672974064328, 2.168404344971008868E-16 ) ) ;
#169=EDGE_LOOP ( 'NONE', ( #15590, #17525, #15025, #11757 ) ) ;
#183=CLOSED_SHELL ( 'NONE', ( #8623, #12070, #5801, #4336, #16789, #13518, #7804, #15959, #10685, #12852, #17802, #16024, #17150, #1736, #8963, #16034, #14996, #8741, #15227, #15885, #6061, #555, #6136, #15606, #14685, #7463, #6386 ) ) ;
#198=DIRECTION ( 'NONE',  ( -1.000000000000000000, -0.000000000000000000, -0.000000000000000000 ) ) ;
#204=VECTOR ( 'NONE', #11238, 1000.000000000000227 ) ;
#260=DIRECTION ( 'NONE',  ( -0.000000000000000000, -1.000000000000000000, 1.502314598737159031E-16 ) ) ;
#278=VERTEX_POINT ( 'NONE', #11912 ) ;
#283=AXIS2_PLACEMENT_3D ( 'NONE', #4294, #5954, #10212 ) ;
#353=PLANE ( 'NONE',  #5705 ) ;
#354=CARTESIAN_POINT ( 'NONE',  ( 1.300000000000000044, 0.000000000000000000, 0.000000000000000000 ) ) ;
#361=CIRCLE ( 'NONE', #2453, 1.610000000000000098 ) ;
#371=ORIENTED_EDGE ( 'NONE', *, *, #11937, .T. ) ;
#389=DIRECTION ( 'NONE',  ( 0.000000000000000000, 0.000000000000000000, 1.000000000000000000 ) ) ;
#404=CIRCLE ( 'NONE', #10754, 2.000000000000000444 ) ;
#410=ORIENTED_EDGE ( 'NONE', *, *, #11507, .T. ) ;
#445=DIRECTION ( 'NONE',  ( -0.000000000000000000, 0.000000000000000000, -1.000000000000000000 ) ) ;
#481=ORIENTED_EDGE ( 'NONE', *, *, #17047, .T. ) ;
#510=DIRECTION ( 'NONE',  ( -1.000000000000000000, -0.000000000000000000, -0.000000000000000000 ) ) ;
#521=LINE ( 'NONE', #2012, #6452 ) ;
#531=CIRCLE ( 'NONE', #12662, 1.250000000000000222 ) ;
#546=ORIENTED_EDGE ( 'NONE', *, *, #16871, .T. ) ;
#551=ORIENTED_EDGE ( 'NONE', *, *, #7099, .T. ) ;
#555=ADVANCED_FACE ( 'NONE', ( #15075 ), #3750, .F. ) ;
#596=ORIENTED_EDGE ( 'NONE', *, *, #6615, .F. ) ;
#610=VECTOR ( 'NONE', #3816, 1000.000000000000227 ) ;
#612=EDGE_CURVE ( 'NONE', #11658, #10194, #17872, .T. ) ;
#716=SHAPE_DEFINITION_REPRESENTATION ( #7507, #1416 ) ;
#728=DIRECTION ( 'NONE',  ( 0.000000000000000000, 0.000000000000000000, 1.000000000000000000 ) ) ;
#786=EDGE_CURVE ( 'NONE', #17921, #15490, #9461, .T. ) ;
#811=DIRECTION ( 'NONE',  ( -0.000000000000000000, -0.5000000000000002220, -0.8660254037844384856 ) ) ;
#824=ORIENTED_EDGE ( 'NONE', *, *, #8075, .T. ) ;
#878=DIRECTION ( 'NONE',  ( 0.000000000000000000, 0.000000000000000000, 1.000000000000000000 ) ) ;
#959=CARTESIAN_POINT ( 'NONE',  ( 1.300000000000000044, 1.443375672974065216, 7.222237291452134449E-31 ) ) ;
#1083=VERTEX_POINT ( 'NONE', #5400 ) ;
#1091=CARTESIAN_POINT ( 'NONE',  ( 1.300000000000000044, -0.7216878364870317197, -1.250000000000000000 ) ) ;
#1118=DIRECTION ( 'NONE',  ( -0.000000000000000000, 1.000000000000000000, -0.000000000000000000 ) ) ;
#1125=ORIENTED_EDGE ( 'NONE', *, *, #2773, .F. ) ;
#1208=AXIS2_PLACEMENT_3D ( 'NONE', #15326, #2625, #8266 ) ;
#1215=CARTESIAN_POINT ( 'NONE',  ( 2.399999999999999911, 2.449293598294706414E-16, -2.000000000000000000 ) ) ;
#1249=LINE ( 'NONE', #12540, #15570 ) ;
#1260=COLOUR_RGB ( '',1.000000000000000000, 0.9490196078431372140, 0.9098039215686274384 ) ;
#1319=CARTESIAN_POINT ( 'NONE',  ( 14.20000000000000107, 2.210487472460972698E-16, -1.610000000000000098 ) ) ;
#1322=STYLED_ITEM('',(#18417),#8321);
#1324=DIRECTION ( 'NONE',  ( 0.000000000000000000, 0.000000000000000000, 1.000000000000000000 ) ) ;
#1332=ORIENTED_EDGE ( 'NONE', *, *, #11015, .T. ) ;
#1370=( NAMED_UNIT ( * ) SI_UNIT ( $, .STERADIAN. ) SOLID_ANGLE_UNIT ( ) );
#1402=VERTEX_POINT ( 'NONE', #6122 ) ;
#1416=SHAPE_REPRESENTATION ( 'socket button head screw_iso_ISO 7380 - M4 x 12 - 12N', ( #16940 ), #8637 ) ;
#1449=EDGE_CURVE ( 'NONE', #3078, #1717, #16362, .T. ) ;
#1475=DIRECTION ( 'NONE',  ( -1.000000000000000000, -0.000000000000000000, -0.000000000000000000 ) ) ;
#1482=FACE_OUTER_BOUND ( 'NONE', #12182, .T. ) ;
#1503=EDGE_CURVE ( 'NONE', #4478, #6078, #16156, .T. ) ;
#1514=CARTESIAN_POINT ( 'NONE',  ( 1.300000000000000044, 1.443375672974065216, 7.222237291452134449E-31 ) ) ;
#1573=DIRECTION ( 'NONE',  ( -1.000000000000000000, -0.000000000000000000, -0.000000000000000000 ) ) ;
#1604=CONICAL_SURFACE ( 'NONE', #12245, 1.610000000000000098, 0.7853981633974469467 ) ;
#1621=ORIENTED_EDGE ( 'NONE', *, *, #7906, .T. ) ;
#1657=ORIENTED_EDGE ( 'NONE', *, *, #3378, .T. ) ;
#1682=VERTEX_POINT ( 'NONE', #16980 ) ;
#1690=CYLINDRICAL_SURFACE ( 'NONE', #91, 2.000000000000000000 ) ;
#1717=VERTEX_POINT ( 'NONE', #8503 ) ;
#1727=LINE ( 'NONE', #7361, #2899 ) ;
#1736=ADVANCED_FACE ( 'NONE', ( #1482 ), #16973, .F. ) ;
#1738=EDGE_CURVE ( 'NONE', #8602, #11760, #86, .T. ) ;
#1746=ORIENTED_EDGE ( 'NONE', *, *, #2967, .F. ) ;
#1781=FACE_BOUND ( 'NONE', #14611, .T. ) ;
#1801=DIRECTION ( 'NONE',  ( -1.000000000000000000, 0.000000000000000000, 0.000000000000000000 ) ) ;
#1902=EDGE_LOOP ( 'NONE', ( #12853, #6335, #1332, #1746, #7433 ) ) ;
#1922=DIRECTION ( 'NONE',  ( 0.000000000000000000, 0.000000000000000000, 1.000000000000000000 ) ) ;
#1937=ORIENTED_EDGE ( 'NONE', *, *, #18156, .T. ) ;
#1971=ORIENTED_EDGE ( 'NONE', *, *, #14248, .T. ) ;
#1991=LINE ( 'NONE', #9199, #10964 ) ;
#2008=VECTOR ( 'NONE', #15096, 1000.000000000000000 ) ;
#2012=CARTESIAN_POINT ( 'NONE',  ( 1.300000000000000044, 1.443375672974065216, 7.222237291452134449E-31 ) ) ;
#2025=EDGE_CURVE ( 'NONE', #15490, #11760, #15195, .T. ) ;
#2055=EDGE_LOOP ( 'NONE', ( #8033, #8313, #8249, #18260 ) ) ;
#2100=CIRCLE ( 'NONE', #20, 1.250000000000000222 ) ;
#2112=ORIENTED_EDGE ( 'NONE', *, *, #2025, .F. ) ;
#2129=LINE ( 'NONE', #1091, #2008 ) ;
#2132=LINE ( 'NONE', #6379, #10387 ) ;
#2148=CARTESIAN_POINT ( 'NONE',  ( 2.200000000000000178, 0.000000000000000000, 3.799999999999999378 ) ) ;
#2149=CIRCLE ( 'NONE', #11901, 3.799999999999999378 ) ;
#2155=EDGE_CURVE ( 'NONE', #15759, #4478, #2720, .T. ) ;
#2177=AXIS2_PLACEMENT_3D ( 'NONE', #14843, #4525, #1324 ) ;
#2216=LINE ( 'NONE', #12198, #5203 ) ;
#2243=PLANE ( 'NONE',  #7359 ) ;
#2264=AXIS2_PLACEMENT_3D ( 'NONE', #115, #15695, #2993 ) ;
#2453=AXIS2_PLACEMENT_3D ( 'NONE', #14576, #8898, #389 ) ;
#2463=EDGE_CURVE ( 'NONE', #9743, #17585, #13813, .T. ) ;
#2487=DIRECTION ( 'NONE',  ( -1.000000000000000000, -0.000000000000000000, -0.000000000000000000 ) ) ;
#2515=DIRECTION ( 'NONE',  ( 0.000000000000000000, 0.000000000000000000, 1.000000000000000000 ) ) ;
#2625=DIRECTION ( 'NONE',  ( -1.000000000000000000, 0.000000000000000000, -0.000000000000000000 ) ) ;
#2665=AXIS2_PLACEMENT_3D ( 'NONE', #15563, #11280, #2515 ) ;
#2708=CIRCLE ( 'NONE', #3582, 1.250000000000000222 ) ;
#2720=LINE ( 'NONE', #14102, #15780 ) ;
#2770=EDGE_CURVE ( 'NONE', #8355, #13335, #361, .T. ) ;
#2773=EDGE_CURVE ( 'NONE', #1402, #3198, #12787, .T. ) ;
#2870=CARTESIAN_POINT ( 'NONE',  ( 8.673617379884035472E-16, -1.899999999999999689, -3.490243377569955568E-16 ) ) ;
#2891=EDGE_LOOP ( 'NONE', ( #2922, #16866, #14458, #10653, #17939 ) ) ;
#2899=VECTOR ( 'NONE', #10426, 1000.000000000000227 ) ;
#2910=CARTESIAN_POINT ( 'NONE',  ( 0.000000000000000000, 0.000000000000000000, 0.000000000000000000 ) ) ;
#2922=ORIENTED_EDGE ( 'NONE', *, *, #2463, .F. ) ;
#2926=DIRECTION ( 'NONE',  ( -0.000000000000000000, -0.5000000000000002220, -0.8660254037844384856 ) ) ;
#2930=CARTESIAN_POINT ( 'NONE',  ( 1.300000000000000044, -0.7216878364870317197, 1.250000000000000000 ) ) ;
#2956=ORIENTED_EDGE ( 'NONE', *, *, #4312, .T. ) ;
#2967=EDGE_CURVE ( 'NONE', #13882, #9022, #16517, .T. ) ;
#2993=DIRECTION ( 'NONE',  ( -0.000000000000000000, 0.000000000000000000, -1.000000000000000000 ) ) ;
#3000=LINE ( 'NONE', #7432, #14471 ) ;
#3073=EDGE_CURVE ( 'NONE', #9202, #3078, #9631, .T. ) ;
#3078=VERTEX_POINT ( 'NONE', #1215 ) ;
#3115=DIRECTION ( 'NONE',  ( 0.000000000000000000, 0.000000000000000000, 1.000000000000000000 ) ) ;
#3127=ORIENTED_EDGE ( 'NONE', *, *, #8075, .F. ) ;
#3198=VERTEX_POINT ( 'NONE', #2870 ) ;
#3203=EDGE_CURVE ( 'NONE', #7786, #17921, #2149, .T. ) ;
#3235=ORIENTED_EDGE ( 'NONE', *, *, #10761, .F. ) ;
#3241=CARTESIAN_POINT ( 'NONE',  ( 1.300000000000000044, 0.7216878364870329410, 1.249999999999999778 ) ) ;
#3243=CIRCLE ( 'NONE', #3812, 1.250000000000000222 ) ;
#3254=AXIS2_PLACEMENT_3D ( 'NONE', #4425, #13043, #17344 ) ;
#3261=DIRECTION ( 'NONE',  ( 0.000000000000000000, 0.000000000000000000, 1.000000000000000000 ) ) ;
#3264=DIRECTION ( 'NONE',  ( 1.000000000000000000, 0.000000000000000000, 0.000000000000000000 ) ) ;
#3286=ORIENTED_EDGE ( 'NONE', *, *, #17047, .F. ) ;
#3300=DIRECTION ( 'NONE',  ( 0.000000000000000000, 0.000000000000000000, 1.000000000000000000 ) ) ;
#3378=EDGE_CURVE ( 'NONE', #6052, #11658, #13147, .T. ) ;
#3425=EDGE_LOOP ( 'NONE', ( #17917, #15285, #1937, #1125, #8932 ) ) ;
#3448=DIRECTION ( 'NONE',  ( -0.000000000000000000, 0.5000000000000002220, -0.8660254037844384856 ) ) ;
#3503=CARTESIAN_POINT ( 'NONE',  ( 13.80999999999999872, 2.449293598294706907E-16, -2.000000000000000444 ) ) ;
#3533=CIRCLE ( 'NONE', #8263, 2.000000000000000000 ) ;
#3551=AXIS2_PLACEMENT_3D ( 'NONE', #12405, #18096, #5368 ) ;
#3582=AXIS2_PLACEMENT_3D ( 'NONE', #3866, #7761, #6284 ) ;
#3587=ORIENTED_EDGE ( 'NONE', *, *, #11512, .T. ) ;
#3656=VECTOR ( 'NONE', #13907, 1000.000000000000000 ) ;
#3681=DIRECTION ( 'NONE',  ( 0.000000000000000000, 0.000000000000000000, 1.000000000000000000 ) ) ;
#3720=AXIS2_PLACEMENT_3D ( 'NONE', #16763, #2487, #3681 ) ;
#3725=FACE_OUTER_BOUND ( 'NONE', #17989, .T. ) ;
#3728=VERTEX_POINT ( 'NONE', #4143 ) ;
#3750=PLANE ( 'NONE',  #5313 ) ;
#3774=ORIENTED_EDGE ( 'NONE', *, *, #5682, .F. ) ;
#3775=VECTOR ( 'NONE', #5436, 1000.000000000000000 ) ;
#3787=CARTESIAN_POINT ( 'NONE',  ( 0.000000000000000000, 0.7216878364870329410, 1.249999999999999778 ) ) ;
#3812=AXIS2_PLACEMENT_3D ( 'NONE', #354, #10160, #7285 ) ;
#3816=DIRECTION ( 'NONE',  ( -0.000000000000000000, 0.5000000000000000000, 0.8660254037844385966 ) ) ;
#3866=CARTESIAN_POINT ( 'NONE',  ( 1.300000000000000044, 0.000000000000000000, 0.000000000000000000 ) ) ;
#3915=DIRECTION ( 'NONE',  ( -1.000000000000000000, -0.000000000000000000, -0.000000000000000000 ) ) ;
#3962=SURFACE_STYLE_USAGE ( .BOTH. , #8481 ) ;
#3977=PRODUCT ( 'socket button head screw_iso_ISO 7380 - M4 x 12 - 12N', 'socket button head screw_iso_ISO 7380 - M4 x 12 - 12N', '', ( #13489 ) ) ;
#4012=ORIENTED_EDGE ( 'NONE', *, *, #12319, .F. ) ;
#4028=AXIS2_PLACEMENT_3D ( 'NONE', #5994, #14351, #7199 ) ;
#4046=FILL_AREA_STYLE ('',( #4145 ) ) ;
#4077=AXIS2_PLACEMENT_3D ( 'NONE', #81, #14651, #12186 ) ;
#4085=EDGE_CURVE ( 'NONE', #9743, #1083, #9593, .T. ) ;
#4108=VECTOR ( 'NONE', #14757, 1000.000000000000000 ) ;
#4143=CARTESIAN_POINT ( 'NONE',  ( 0.000000000000000000, 1.443375672974065216, 7.222237291452134449E-31 ) ) ;
#4144=EDGE_CURVE ( 'NONE', #17585, #6078, #11324, .T. ) ;
#4145=FILL_AREA_STYLE_COLOUR ( '', #1260 ) ;
#4167=CARTESIAN_POINT ( 'NONE',  ( 0.000000000000000000, -0.7216878364870317197, -1.250000000000000000 ) ) ;
#4198=CARTESIAN_POINT ( 'NONE',  ( 1.300000000000000044, -1.082531754730548412, -0.6250000000000003331 ) ) ;
#4214=DIRECTION ( 'NONE',  ( 0.000000000000000000, 0.000000000000000000, 1.000000000000000000 ) ) ;
#4215=EDGE_CURVE ( 'NONE', #8977, #11296, #11590, .T. ) ;
#4239=CARTESIAN_POINT ( 'NONE',  ( 2.199999999999999734, 0.000000000000000000, 2.200000000000000178 ) ) ;
#4294=CARTESIAN_POINT ( 'NONE',  ( 1.820000000000000062, 0.000000000000000000, 0.000000000000000000 ) ) ;
#4305=CARTESIAN_POINT ( 'NONE',  ( 1.300000000000000044, -1.443375672974064328, 1.278502688459867223E-18 ) ) ;
#4312=EDGE_CURVE ( 'NONE', #6560, #8602, #13107, .T. ) ;
#4329=DIRECTION ( 'NONE',  ( 1.000000000000000000, 0.000000000000000000, -0.000000000000000000 ) ) ;
#4336=ADVANCED_FACE ( 'NONE', ( #14386 ), #1690, .T. ) ;
#4393=CIRCLE ( 'NONE', #5287, 3.799999999999999378 ) ;
#4425=CARTESIAN_POINT ( 'NONE',  ( 2.199999999999999734, 0.000000000000000000, 0.000000000000000000 ) ) ;
#4478=VERTEX_POINT ( 'NONE', #13265 ) ;
#4497=FACE_OUTER_BOUND ( 'NONE', #7435, .T. ) ;
#4525=DIRECTION ( 'NONE',  ( -1.000000000000000000, -0.000000000000000000, -0.000000000000000000 ) ) ;
#4546=DIRECTION ( 'NONE',  ( -1.000000000000000000, 0.000000000000000000, -0.000000000000000000 ) ) ;
#4727=AXIS2_PLACEMENT_3D ( 'NONE', #14450, #5905, #11554 ) ;
#4741=DIRECTION ( 'NONE',  ( -1.000000000000000000, 0.000000000000000000, 0.000000000000000000 ) ) ;
#4793=CARTESIAN_POINT ( 'NONE',  ( 1.820000000000000062, 3.799999999999999378, 0.000000000000000000 ) ) ;
#4858=AXIS2_PLACEMENT_3D ( 'NONE', #6246, #17595, #10510 ) ;
#4883=DIRECTION ( 'NONE',  ( 1.000000000000000000, 0.000000000000000000, 0.000000000000000000 ) ) ;
#4908=FACE_OUTER_BOUND ( 'NONE', #18193, .T. ) ;
#4965=VECTOR ( 'NONE', #5690, 1000.000000000000000 ) ;
#4967=VERTEX_POINT ( 'NONE', #4239 ) ;
#4971=CARTESIAN_POINT ( 'NONE',  ( 4.336808689942017736E-16, 0.000000000000000000, 0.000000000000000000 ) ) ;
#4972=FACE_OUTER_BOUND ( 'NONE', #6672, .T. ) ;
#5027=LINE ( 'NONE', #16353, #17751 ) ;
#5108=APPLICATION_CONTEXT ( 'automotive_design' ) ;
#5111=DIRECTION ( 'NONE',  ( -1.000000000000000000, -0.000000000000000000, -0.000000000000000000 ) ) ;
#5141=CARTESIAN_POINT ( 'NONE',  ( 1.300000000000000044, 0.7216878364870329410, 1.249999999999999778 ) ) ;
#5168=ORIENTED_EDGE ( 'NONE', *, *, #4144, .T. ) ;
#5203=VECTOR ( 'NONE', #811, 1000.000000000000114 ) ;
#5208=VECTOR ( 'NONE', #13137, 1000.000000000000000 ) ;
#5231=EDGE_LOOP ( 'NONE', ( #1657, #11566, #1971, #11980, #9172 ) ) ;
#5246=ORIENTED_EDGE ( 'NONE', *, *, #2025, .T. ) ;
#5251=DIRECTION ( 'NONE',  ( 0.000000000000000000, -1.502314598737159031E-16, -1.000000000000000000 ) ) ;
#5273=VECTOR ( 'NONE', #17389, 1000.000000000000000 ) ;
#5287=AXIS2_PLACEMENT_3D ( 'NONE', #7405, #17078, #15581 ) ;
#5313=AXIS2_PLACEMENT_3D ( 'NONE', #10981, #12184, #12454 ) ;
#5346=EDGE_CURVE ( 'NONE', #10567, #9202, #404, .T. ) ;
#5356=PRESENTATION_STYLE_ASSIGNMENT (( #3962 ) ) ;
#5368=DIRECTION ( 'NONE',  ( -0.000000000000000000, 0.000000000000000000, -1.000000000000000000 ) ) ;
#5400=CARTESIAN_POINT ( 'NONE',  ( 1.300000000000000044, 1.877893248421448789E-16, 1.250000000000000000 ) ) ;
#5435=DIRECTION ( 'NONE',  ( -1.000000000000000000, -0.000000000000000000, -0.000000000000000000 ) ) ;
#5436=DIRECTION ( 'NONE',  ( -1.000000000000000000, -0.000000000000000000, -0.000000000000000000 ) ) ;
#5503=CARTESIAN_POINT ( 'NONE',  ( 2.399999999999999911, 0.000000000000000000, 2.200000000000000178 ) ) ;
#5513=DIRECTION ( 'NONE',  ( -1.000000000000000000, -0.000000000000000000, -0.000000000000000000 ) ) ;
#5574=ORIENTED_EDGE ( 'NONE', *, *, #13117, .T. ) ;
#5577=DIRECTION ( 'NONE',  ( 0.000000000000000000, 0.000000000000000000, 1.000000000000000000 ) ) ;
#5617=LINE ( 'NONE', #18166, #3775 ) ;
#5682=EDGE_CURVE ( 'NONE', #9202, #10567, #8102, .T. ) ;
#5690=DIRECTION ( 'NONE',  ( -1.000000000000000000, 0.000000000000000000, 0.000000000000000000 ) ) ;
#5704=EDGE_CURVE ( 'NONE', #6724, #3078, #17309, .T. ) ;
#5705=AXIS2_PLACEMENT_3D ( 'NONE', #4971, #10444, #16121 ) ;
#5713=VECTOR ( 'NONE', #15082, 1000.000000000000114 ) ;
#5730=CARTESIAN_POINT ( 'NONE',  ( 0.000000000000000000, -0.7216878364870317197, 1.250000000000000000 ) ) ;
#5739=CARTESIAN_POINT ( 'NONE',  ( 2.399999999999999911, 0.000000000000000000, 0.000000000000000000 ) ) ;
#5791=DIRECTION ( 'NONE',  ( 0.000000000000000000, 1.000000000000000000, 0.000000000000000000 ) ) ;
#5795=LINE ( 'NONE', #11438, #7122 ) ;
#5801=ADVANCED_FACE ( 'NONE', ( #16554 ), #1604, .T. ) ;
#5819=FACE_OUTER_BOUND ( 'NONE', #3425, .T. ) ;
#5838=ORIENTED_EDGE ( 'NONE', *, *, #7896, .T. ) ;
#5883=PLANE ( 'NONE',  #7689 ) ;
#5905=DIRECTION ( 'NONE',  ( 1.000000000000000000, 0.000000000000000000, -0.000000000000000000 ) ) ;
#5939=AXIS2_PLACEMENT_3D ( 'NONE', #16106, #11534, #10331 ) ;
#5954=DIRECTION ( 'NONE',  ( -1.000000000000000000, -0.000000000000000000, -0.000000000000000000 ) ) ;
#5977=FACE_OUTER_BOUND ( 'NONE', #16084, .T. ) ;
#5994=CARTESIAN_POINT ( 'NONE',  ( 1.300000000000000044, -1.443375672974064328, 1.278502688459867223E-18 ) ) ;
#6024=FACE_OUTER_BOUND ( 'NONE', #11846, .T. ) ;
#6025=ORIENTED_EDGE ( 'NONE', *, *, #2773, .T. ) ;
#6052=VERTEX_POINT ( 'NONE', #1514 ) ;
#6058=ORIENTED_EDGE ( 'NONE', *, *, #11239, .T. ) ;
#6061=ADVANCED_FACE ( 'NONE', ( #10019 ), #8537, .F. ) ;
#6078=VERTEX_POINT ( 'NONE', #4198 ) ;
#6122=CARTESIAN_POINT ( 'NONE',  ( 8.673617379884035472E-16, 1.899999999999999689, 0.000000000000000000 ) ) ;
#6136=ADVANCED_FACE ( 'NONE', ( #7147 ), #7238, .F. ) ;
#6142=AXIS2_PLACEMENT_3D ( 'NONE', #17845, #5111, #17935 ) ;
#6153=DIRECTION ( 'NONE',  ( 0.000000000000000000, 0.000000000000000000, 1.000000000000000000 ) ) ;
#6246=CARTESIAN_POINT ( 'NONE',  ( 2.399999999999999911, 2.694222958124177006E-16, -2.200000000000000178 ) ) ;
#6276=CARTESIAN_POINT ( 'NONE',  ( 1.300000000000000044, 0.7216878364870329410, -1.250000000000000000 ) ) ;
#6284=DIRECTION ( 'NONE',  ( 0.000000000000000000, 0.000000000000000000, 1.000000000000000000 ) ) ;
#6315=CARTESIAN_POINT ( 'NONE',  ( 2.399999999999999911, 0.000000000000000000, 0.000000000000000000 ) ) ;
#6335=ORIENTED_EDGE ( 'NONE', *, *, #16935, .T. ) ;
#6357=CARTESIAN_POINT ( 'NONE',  ( 3.885274725274725949, -4.336808689942017736E-16, 0.000000000000000000 ) ) ;
#6379=CARTESIAN_POINT ( 'NONE',  ( 1.300000000000000044, -0.7216878364870317197, 1.250000000000000000 ) ) ;
#6386=ADVANCED_FACE ( 'NONE', ( #10959 ), #9933, .F. ) ;
#6419=DIRECTION ( 'NONE',  ( -0.000000000000000000, 0.5000000000000002220, -0.8660254037844384856 ) ) ;
#6428=DIRECTION ( 'NONE',  ( 1.000000000000000000, 0.000000000000000000, 0.000000000000000000 ) ) ;
#6452=VECTOR ( 'NONE', #11532, 1000.000000000000000 ) ;
#6456=ORIENTED_EDGE ( 'NONE', *, *, #612, .F. ) ;
#6560=VERTEX_POINT ( 'NONE', #13843 ) ;
#6579=DIRECTION ( 'NONE',  ( -0.000000000000000000, 0.5000000000000002220, -0.8660254037844384856 ) ) ;
#6605=EDGE_LOOP ( 'NONE', ( #14810, #5838, #14288, #551, #17439, #8398 ) ) ;
#6615=EDGE_CURVE ( 'NONE', #17585, #8977, #1249, .T. ) ;
#6668=ORIENTED_EDGE ( 'NONE', *, *, #15462, .F. ) ;
#6672=EDGE_LOOP ( 'NONE', ( #5574, #16692, #11138, #9423, #7931 ) ) ;
#6724=VERTEX_POINT ( 'NONE', #8719 ) ;
#6749=FACE_OUTER_BOUND ( 'NONE', #11199, .T. ) ;
#6751=DIRECTION ( 'NONE',  ( 0.000000000000000000, -0.5000000000000000000, -0.8660254037844385966 ) ) ;
#6755=ORIENTED_EDGE ( 'NONE', *, *, #12262, .T. ) ;
#6793=CIRCLE ( 'NONE', #15416, 1.899999999999999689 ) ;
#6795=CARTESIAN_POINT ( 'NONE',  ( 14.20000000000000107, 0.000000000000000000, 0.000000000000000000 ) ) ;
#6845=CARTESIAN_POINT ( 'NONE',  ( 14.20000000000000107, 0.000000000000000000, 0.000000000000000000 ) ) ;
#6896=EDGE_CURVE ( 'NONE', #11760, #7786, #4393, .T. ) ;
#6916=PRODUCT_DEFINITION_CONTEXT ( 'detailed design', #5108, 'design' ) ;
#6973=DIRECTION ( 'NONE',  ( 0.000000000000000000, 0.000000000000000000, -1.000000000000000000 ) ) ;
#6978=EDGE_LOOP ( 'NONE', ( #9490, #3127, #16119 ) ) ;
#7016=LINE ( 'NONE', #9808, #16262 ) ;
#7058=AXIS2_PLACEMENT_3D ( 'NONE', #6276, #728, #16208 ) ;
#7099=EDGE_CURVE ( 'NONE', #9022, #11296, #7864, .T. ) ;
#7122=VECTOR ( 'NONE', #17129, 1000.000000000000000 ) ;
#7147=FACE_OUTER_BOUND ( 'NONE', #16231, .T. ) ;
#7199=DIRECTION ( 'NONE',  ( 0.000000000000000000, 0.5000000000000002220, 0.8660254037844384856 ) ) ;
#7211=CARTESIAN_POINT ( 'NONE',  ( 0.000000000000000000, 0.000000000000000000, 3.799999999999999378 ) ) ;
#7238=PLANE ( 'NONE',  #2264 ) ;
#7263=CIRCLE ( 'NONE', #9589, 3.799999999999999378 ) ;
#7285=DIRECTION ( 'NONE',  ( 0.000000000000000000, 0.000000000000000000, 1.000000000000000000 ) ) ;
#7289=LINE ( 'NONE', #5730, #8206 ) ;
#7297=DIRECTION ( 'NONE',  ( 0.000000000000000000, 0.000000000000000000, 1.000000000000000000 ) ) ;
#7359=AXIS2_PLACEMENT_3D ( 'NONE', #10836, #7962, #7867 ) ;
#7361=CARTESIAN_POINT ( 'NONE',  ( 1.300000000000000044, 1.443375672974065216, 7.222237291452134449E-31 ) ) ;
#7378=FACE_BOUND ( 'NONE', #6605, .T. ) ;
#7382=CARTESIAN_POINT ( 'NONE',  ( 4.336808689942017736E-16, -0.7216878364870317197, 1.250000000000000000 ) ) ;
#7387=EDGE_CURVE ( 'NONE', #3728, #278, #15026, .T. ) ;
#7405=CARTESIAN_POINT ( 'NONE',  ( 1.820000000000000062, 0.000000000000000000, 0.000000000000000000 ) ) ;
#7421=CARTESIAN_POINT ( 'NONE',  ( 1.300000000000000044, 0.7216878364870329410, -1.250000000000000000 ) ) ;
#7432=CARTESIAN_POINT ( 'NONE',  ( 1.300000000000000044, -1.443375672974064328, 1.278502688459867223E-18 ) ) ;
#7433=ORIENTED_EDGE ( 'NONE', *, *, #12262, .F. ) ;
#7435=EDGE_LOOP ( 'NONE', ( #16730, #5246, #7698, #8830, #12884 ) ) ;
#7457=DIRECTION ( 'NONE',  ( 0.000000000000000000, 0.000000000000000000, -1.000000000000000000 ) ) ;
#7463=ADVANCED_FACE ( 'NONE', ( #6749 ), #16788, .F. ) ;
#7507=PRODUCT_DEFINITION_SHAPE ( 'NONE', 'NONE',  #12171 ) ;
#7515=CARTESIAN_POINT ( 'NONE',  ( 1.300000000000000044, -0.7216878364870317197, -1.250000000000000000 ) ) ;
#7548=CARTESIAN_POINT ( 'NONE',  ( 1.300000000000000044, -0.7216878364870317197, -1.250000000000000000 ) ) ;
#7554=ORIENTED_EDGE ( 'NONE', *, *, #13117, .F. ) ;
#7654=AXIS2_PLACEMENT_3D ( 'NONE', #11101, #4329, #445 ) ;
#7657=LINE ( 'NONE', #17433, #5208 ) ;
#7663=VECTOR ( 'NONE', #2926, 1000.000000000000114 ) ;
#7689=AXIS2_PLACEMENT_3D ( 'NONE', #7548, #10232, #11349 ) ;
#7696=DIRECTION ( 'NONE',  ( 1.000000000000000000, 0.000000000000000000, 0.000000000000000000 ) ) ;
#7698=ORIENTED_EDGE ( 'NONE', *, *, #6896, .T. ) ;
#7761=DIRECTION ( 'NONE',  ( -1.000000000000000000, -0.000000000000000000, -0.000000000000000000 ) ) ;
#7781=DIRECTION ( 'NONE',  ( 0.000000000000000000, 0.000000000000000000, 1.000000000000000000 ) ) ;
#7786=VERTEX_POINT ( 'NONE', #4793 ) ;
#7804=ADVANCED_FACE ( 'NONE', ( #17530, #7378 ), #353, .T. ) ;
#7864=LINE ( 'NONE', #10470, #4108 ) ;
#7867=DIRECTION ( 'NONE',  ( 0.000000000000000000, 0.5000000000000001110, -0.8660254037844385966 ) ) ;
#7890=CARTESIAN_POINT ( 'NONE',  ( 1.300000000000000044, 0.000000000000000000, 0.000000000000000000 ) ) ;
#7891=DIRECTION ( 'NONE',  ( -0.7071067811865484609, 0.000000000000000000, 0.7071067811865465735 ) ) ;
#7896=EDGE_CURVE ( 'NONE', #15565, #13882, #2216, .T. ) ;
#7906=EDGE_CURVE ( 'NONE', #4967, #6724, #11404, .T. ) ;
#7914=CARTESIAN_POINT ( 'NONE',  ( 1.820000000000000062, 0.000000000000000000, 3.799999999999999378 ) ) ;
#7931=ORIENTED_EDGE ( 'NONE', *, *, #11015, .F. ) ;
#7962=DIRECTION ( 'NONE',  ( 0.000000000000000000, -0.8660254037844385966, -0.5000000000000001110 ) ) ;
#8033=ORIENTED_EDGE ( 'NONE', *, *, #5346, .T. ) ;
#8064=VECTOR ( 'NONE', #13426, 1000.000000000000000 ) ;
#8075=EDGE_CURVE ( 'NONE', #16110, #15759, #16854, .T. ) ;
#8102=CIRCLE ( 'NONE', #11643, 2.000000000000000444 ) ;
#8142=DIRECTION ( 'NONE',  ( 0.000000000000000000, 0.000000000000000000, 1.000000000000000000 ) ) ;
#8188=APPLICATION_CONTEXT ( 'automotive_design' ) ;
#8203=ORIENTED_EDGE ( 'NONE', *, *, #5704, .F. ) ;
#8206=VECTOR ( 'NONE', #260, 1000.000000000000000 ) ;
#8249=ORIENTED_EDGE ( 'NONE', *, *, #1449, .T. ) ;
#8263=AXIS2_PLACEMENT_3D ( 'NONE', #12199, #4883, #10535 ) ;
#8266=DIRECTION ( 'NONE',  ( -0.000000000000000000, 0.000000000000000000, 1.000000000000000000 ) ) ;
#8279=AXIS2_PLACEMENT_3D ( 'NONE', #6845, #1475, #8770 ) ;
#8313=ORIENTED_EDGE ( 'NONE', *, *, #3073, .T. ) ;
#8321=MANIFOLD_SOLID_BREP ( 'Hex', #183 ) ;
#8355=VERTEX_POINT ( 'NONE', #1319 ) ;
#8373=DIRECTION ( 'NONE',  ( -1.000000000000000000, -0.000000000000000000, -0.000000000000000000 ) ) ;
#8388=DIRECTION ( 'NONE',  ( 0.000000000000000000, 1.000000000000000000, -1.502314598737159031E-16 ) ) ;
#8398=ORIENTED_EDGE ( 'NONE', *, *, #7387, .T. ) ;
#8481=SURFACE_SIDE_STYLE ('',( #15641 ) ) ;
#8503=CARTESIAN_POINT ( 'NONE',  ( 2.399999999999999911, 0.000000000000000000, 2.000000000000000000 ) ) ;
#8537=PLANE ( 'NONE',  #11997 ) ;
#8575=( NAMED_UNIT ( * ) PLANE_ANGLE_UNIT ( ) SI_UNIT ( $, .RADIAN. ) );
#8579=ORIENTED_EDGE ( 'NONE', *, *, #5682, .T. ) ;
#8593=ORIENTED_EDGE ( 'NONE', *, *, #2463, .T. ) ;
#8602=VERTEX_POINT ( 'NONE', #2148 ) ;
#8610=ORIENTED_EDGE ( 'NONE', *, *, #14908, .F. ) ;
#8623=ADVANCED_FACE ( 'NONE', ( #4908 ), #12549, .F. ) ;
#8637=( GEOMETRIC_REPRESENTATION_CONTEXT ( 3 ) GLOBAL_UNCERTAINTY_ASSIGNED_CONTEXT ( ( #17974 ) ) GLOBAL_UNIT_ASSIGNED_CONTEXT ( ( #16959, #8575, #1370 ) ) REPRESENTATION_CONTEXT ( 'NONE', 'WORKASPACE' ) );
#8638=CARTESIAN_POINT ( 'NONE',  ( 1.300000000000000044, -0.7216878364870317197, 1.250000000000000000 ) ) ;
#8657=AXIS2_PLACEMENT_3D ( 'NONE', #17376, #16067, #11777 ) ;
#8674=CARTESIAN_POINT ( 'NONE',  ( 0.000000000000000000, -0.7216878364870317197, -1.250000000000000000 ) ) ;
#8678=ORIENTED_EDGE ( 'NONE', *, *, #13789, .F. ) ;
#8713=DIRECTION ( 'NONE',  ( 0.000000000000000000, 0.000000000000000000, 1.000000000000000000 ) ) ;
#8719=CARTESIAN_POINT ( 'NONE',  ( 2.199999999999999734, 2.694222958124177006E-16, -2.200000000000000178 ) ) ;
#8725=CARTESIAN_POINT ( 'NONE',  ( 14.20000000000000107, 1.971681346627238735E-16, -1.610000000000000098 ) ) ;
#8741=ADVANCED_FACE ( 'NONE', ( #15213 ), #9711, .T. ) ;
#8770=DIRECTION ( 'NONE',  ( 0.000000000000000000, 0.000000000000000000, 1.000000000000000000 ) ) ;
#8797=EDGE_CURVE ( 'NONE', #8602, #6560, #7263, .T. ) ;
#8800=EDGE_LOOP ( 'NONE', ( #17884, #3286, #596 ) ) ;
#8806=ORIENTED_EDGE ( 'NONE', *, *, #1503, .F. ) ;
#8830=ORIENTED_EDGE ( 'NONE', *, *, #14311, .T. ) ;
#8834=CIRCLE ( 'NONE', #16556, 4.324969328314201000 ) ;
#8862=AXIS2_PLACEMENT_3D ( 'NONE', #12565, #5251, #8388 ) ;
#8898=DIRECTION ( 'NONE',  ( -1.000000000000000000, -0.000000000000000000, -0.000000000000000000 ) ) ;
#8932=ORIENTED_EDGE ( 'NONE', *, *, #14311, .F. ) ;
#8935=VECTOR ( 'NONE', #6579, 1000.000000000000114 ) ;
#8963=ADVANCED_FACE ( 'NONE', ( #15652 ), #11552, .T. ) ;
#8977=VERTEX_POINT ( 'NONE', #11649 ) ;
#9022=VERTEX_POINT ( 'NONE', #8674 ) ;
#9024=CARTESIAN_POINT ( 'NONE',  ( 0.000000000000000000, 0.000000000000000000, 0.000000000000000000 ) ) ;
#9098=EDGE_CURVE ( 'NONE', #6560, #17921, #7657, .T. ) ;
#9124=( NAMED_UNIT ( * ) PLANE_ANGLE_UNIT ( ) SI_UNIT ( $, .RADIAN. ) );
#9172=ORIENTED_EDGE ( 'NONE', *, *, #11507, .F. ) ;
#9199=CARTESIAN_POINT ( 'NONE',  ( 1.300000000000000044, -0.7216878364870317197, -1.250000000000000000 ) ) ;
#9202=VERTEX_POINT ( 'NONE', #3503 ) ;
#9276=ORIENTED_EDGE ( 'NONE', *, *, #16871, .F. ) ;
#9330=CARTESIAN_POINT ( 'NONE',  ( 1.300000000000000044, -1.082531754730548190, 0.6250000000000002220 ) ) ;
#9408=AXIS2_PLACEMENT_3D ( 'NONE', #12635, #8373, #18324 ) ;
#9423=ORIENTED_EDGE ( 'NONE', *, *, #7099, .F. ) ;
#9440=DIRECTION ( 'NONE',  ( -0.000000000000000000, -0.5000000000000001110, 0.8660254037844385966 ) ) ;
#9443=CARTESIAN_POINT ( 'NONE',  ( 2.200000000000000178, 0.000000000000000000, 0.000000000000000000 ) ) ;
#9461=CIRCLE ( 'NONE', #283, 3.799999999999999378 ) ;
#9490=ORIENTED_EDGE ( 'NONE', *, *, #11512, .F. ) ;
#9501=ORIENTED_EDGE ( 'NONE', *, *, #3203, .F. ) ;
#9508=CIRCLE ( 'NONE', #16049, 4.324969328314200112 ) ;
#9564=VECTOR ( 'NONE', #10938, 1000.000000000000114 ) ;
#9576=DIRECTION ( 'NONE',  ( -1.000000000000000000, -0.000000000000000000, -0.000000000000000000 ) ) ;
#9589=AXIS2_PLACEMENT_3D ( 'NONE', #9443, #13896, #8142 ) ;
#9593=LINE ( 'NONE', #13670, #5713 ) ;
#9601=AXIS2_PLACEMENT_3D ( 'NONE', #13350, #14948, #7781 ) ;
#9631=LINE ( 'NONE', #12230, #3656 ) ;
#9647=PLANE ( 'NONE',  #1208 ) ;
#9669=DIRECTION ( 'NONE',  ( 0.000000000000000000, -1.000000000000000000, 0.000000000000000000 ) ) ;
#9711=PLANE ( 'NONE',  #14913 ) ;
#9712=CARTESIAN_POINT ( 'NONE',  ( 1.300000000000000044, -0.7216878364870317197, -1.250000000000000000 ) ) ;
#9736=( NAMED_UNIT ( * ) SI_UNIT ( $, .STERADIAN. ) SOLID_ANGLE_UNIT ( ) );
#9743=VERTEX_POINT ( 'NONE', #12749 ) ;
#9808=CARTESIAN_POINT ( 'NONE',  ( 1.300000000000000044, 0.7216878364870329410, -1.250000000000000000 ) ) ;
#9822=VECTOR ( 'NONE', #3448, 1000.000000000000114 ) ;
#9849=AXIS2_PLACEMENT_3D ( 'NONE', #12460, #15174, #17793 ) ;
#9881=SHAPE_REPRESENTATION_RELATIONSHIP ( 'NONE' , 'NONE' ,  #1416, #10928 ) ;
#9933=CONICAL_SURFACE ( 'NONE', #10229, 1732.050807568857181, 1.047197551196592746 ) ;
#9938=FACE_OUTER_BOUND ( 'NONE', #16729, .T. ) ;
#9986=CARTESIAN_POINT ( 'NONE',  ( 1.820000000000000062, 0.000000000000000000, 0.000000000000000000 ) ) ;
#10013=LINE ( 'NONE', #12441, #14469 ) ;
#10019=FACE_OUTER_BOUND ( 'NONE', #8800, .T. ) ;
#10160=DIRECTION ( 'NONE',  ( -1.000000000000000000, -0.000000000000000000, -0.000000000000000000 ) ) ;
#10194=VERTEX_POINT ( 'NONE', #10607 ) ;
#10212=DIRECTION ( 'NONE',  ( 0.000000000000000000, 0.000000000000000000, 1.000000000000000000 ) ) ;
#10229=AXIS2_PLACEMENT_3D ( 'NONE', #16643, #3915, #5577 ) ;
#10232=DIRECTION ( 'NONE',  ( 0.000000000000000000, 0.8660254037844385966, 0.5000000000000003331 ) ) ;
#10233=CARTESIAN_POINT ( 'NONE',  ( 1.300000000000000044, 1.082531754730549300, 0.6250000000000008882 ) ) ;
#10270=ORIENTED_EDGE ( 'NONE', *, *, #12450, .T. ) ;
#10294=TOROIDAL_SURFACE ( 'NONE', #9408, 2.200000000000000178, 0.2000000000000000111 ) ;
#10328=FACE_OUTER_BOUND ( 'NONE', #1902, .T. ) ;
#10331=DIRECTION ( 'NONE',  ( 0.000000000000000000, 0.000000000000000000, 1.000000000000000000 ) ) ;
#10334=ORIENTED_EDGE ( 'NONE', *, *, #16935, .F. ) ;
#10344=CIRCLE ( 'NONE', #8279, 1.610000000000000098 ) ;
#10387=VECTOR ( 'NONE', #17985, 1000.000000000000000 ) ;
#10397=EDGE_CURVE ( 'NONE', #11296, #3728, #14032, .T. ) ;
#10426=DIRECTION ( 'NONE',  ( -0.000000000000000000, 0.5000000000000000000, 0.8660254037844385966 ) ) ;
#10440=EDGE_LOOP ( 'NONE', ( #4012, #15729, #10270, #3774 ) ) ;
#10444=DIRECTION ( 'NONE',  ( -1.000000000000000000, 0.000000000000000000, -0.000000000000000000 ) ) ;
#10470=CARTESIAN_POINT ( 'NONE',  ( 0.000000000000000000, 0.7216878364870329410, -1.250000000000000000 ) ) ;
#10478=ORIENTED_EDGE ( 'NONE', *, *, #17463, .T. ) ;
#10483=EDGE_LOOP ( 'NONE', ( #6025, #15061 ) ) ;
#10510=DIRECTION ( 'NONE',  ( 0.000000000000000000, -1.224646799147353207E-16, 1.000000000000000000 ) ) ;
#10535=DIRECTION ( 'NONE',  ( 0.000000000000000000, 0.000000000000000000, 1.000000000000000000 ) ) ;
#10567=VERTEX_POINT ( 'NONE', #11883 ) ;
#10572=ORIENTED_EDGE ( 'NONE', *, *, #2155, .F. ) ;
#10607=CARTESIAN_POINT ( 'NONE',  ( 1.300000000000000044, 0.7216878364870329410, 1.249999999999999778 ) ) ;
#10612=DIRECTION ( 'NONE',  ( 0.000000000000000000, 1.224646799147353207E-16, -1.000000000000000000 ) ) ;
#10640=ORIENTED_EDGE ( 'NONE', *, *, #11579, .F. ) ;
#10653=ORIENTED_EDGE ( 'NONE', *, *, #17386, .T. ) ;
#10685=ADVANCED_FACE ( 'NONE', ( #3725 ), #12156, .T. ) ;
#10731=ORIENTED_EDGE ( 'NONE', *, *, #1738, .F. ) ;
#10754=AXIS2_PLACEMENT_3D ( 'NONE', #18243, #5513, #4214 ) ;
#10761=EDGE_CURVE ( 'NONE', #278, #15565, #7289, .T. ) ;
#10766=ORIENTED_EDGE ( 'NONE', *, *, #4215, .F. ) ;
#10798=DIRECTION ( 'NONE',  ( -0.000000000000000000, -0.5000000000000001110, 0.8660254037844385966 ) ) ;
#10835=CARTESIAN_POINT ( 'NONE',  ( 1.300000000000000044, 1.443375672974065216, 7.222237291452134449E-31 ) ) ;
#10836=CARTESIAN_POINT ( 'NONE',  ( 1.300000000000000044, 0.7216878364870329410, 1.249999999999999778 ) ) ;
#10883=( GEOMETRIC_REPRESENTATION_CONTEXT ( 3 ) GLOBAL_UNCERTAINTY_ASSIGNED_CONTEXT ( ( #12666 ) ) GLOBAL_UNIT_ASSIGNED_CONTEXT ( ( #17600, #9124, #9736 ) ) REPRESENTATION_CONTEXT ( 'NONE', 'WORKASPACE' ) );
#10928=ADVANCED_BREP_SHAPE_REPRESENTATION ( '', ( #8321, #16940 ), #8637 ) ;
#10938=DIRECTION ( 'NONE',  ( -0.5000000000000042188, 1.060575238724903710E-16, -0.8660254037844361541 ) ) ;
#10959=FACE_OUTER_BOUND ( 'NONE', #2891, .T. ) ;
#10964=VECTOR ( 'NONE', #6419, 1000.000000000000114 ) ;
#10981=CARTESIAN_POINT ( 'NONE',  ( 1.300000000000000044, -1.443375672974064328, 2.168404344971008868E-16 ) ) ;
#11000=EDGE_LOOP ( 'NONE', ( #9276, #8806, #10572 ) ) ;
#11005=( NAMED_UNIT ( * ) SI_UNIT ( $, .STERADIAN. ) SOLID_ANGLE_UNIT ( ) );
#11015=EDGE_CURVE ( 'NONE', #15292, #9022, #2129, .T. ) ;
#11028=ORIENTED_EDGE ( 'NONE', *, *, #5704, .T. ) ;
#11101=CARTESIAN_POINT ( 'NONE',  ( 1.300000000000000044, -1.443375672974064328, 2.168404344971008868E-16 ) ) ;
#11138=ORIENTED_EDGE ( 'NONE', *, *, #4215, .T. ) ;
#11176=AXIS2_PLACEMENT_3D ( 'NONE', #5503, #9669, #6973 ) ;
#11199=EDGE_LOOP ( 'NONE', ( #15328, #7554, #10334 ) ) ;
#11238=DIRECTION ( 'NONE',  ( -0.000000000000000000, 0.5000000000000000000, 0.8660254037844385966 ) ) ;
#11239=EDGE_CURVE ( 'NONE', #10567, #1717, #5617, .T. ) ;
#11241=AXIS2_PLACEMENT_3D ( 'NONE', #16007, #7457, #5791 ) ;
#11280=DIRECTION ( 'NONE',  ( -1.000000000000000000, -0.000000000000000000, -0.000000000000000000 ) ) ;
#11283=EDGE_LOOP ( 'NONE', ( #13893, #15056 ) ) ;
#11296=VERTEX_POINT ( 'NONE', #14143 ) ;
#11324=CIRCLE ( 'NONE', #9849, 1.250000000000000222 ) ;
#11349=DIRECTION ( 'NONE',  ( 0.000000000000000000, -0.5000000000000002220, 0.8660254037844384856 ) ) ;
#11378=DIRECTION ( 'NONE',  ( 0.000000000000000000, 0.000000000000000000, 1.000000000000000000 ) ) ;
#11404=CIRCLE ( 'NONE', #3720, 2.200000000000000178 ) ;
#11407=DIRECTION ( 'NONE',  ( -0.000000000000000000, 1.000000000000000000, -0.000000000000000000 ) ) ;
#11438=CARTESIAN_POINT ( 'NONE',  ( 1.300000000000000044, -0.7216878364870317197, 1.250000000000000000 ) ) ;
#11466=ORIENTED_EDGE ( 'NONE', *, *, #4085, .F. ) ;
#11507=EDGE_CURVE ( 'NONE', #6052, #3728, #521, .T. ) ;
#11512=EDGE_CURVE ( 'NONE', #15759, #1083, #531, .T. ) ;
#11515=ORIENTED_EDGE ( 'NONE', *, *, #3073, .F. ) ;
#11532=DIRECTION ( 'NONE',  ( -1.000000000000000000, 0.000000000000000000, 0.000000000000000000 ) ) ;
#11534=DIRECTION ( 'NONE',  ( -1.000000000000000000, -0.000000000000000000, -0.000000000000000000 ) ) ;
#11552=PLANE ( 'NONE',  #4028 ) ;
#11554=DIRECTION ( 'NONE',  ( -0.000000000000000000, 0.000000000000000000, -1.000000000000000000 ) ) ;
#11566=ORIENTED_EDGE ( 'NONE', *, *, #612, .T. ) ;
#11579=EDGE_CURVE ( 'NONE', #1682, #6052, #1727, .T. ) ;
#11590=LINE ( 'NONE', #7421, #15777 ) ;
#11626=CARTESIAN_POINT ( 'NONE',  ( 14.20000000000000107, 0.000000000000000000, 0.000000000000000000 ) ) ;
#11643=AXIS2_PLACEMENT_3D ( 'NONE', #14609, #510, #6153 ) ;
#11649=CARTESIAN_POINT ( 'NONE',  ( 1.300000000000000044, 0.7216878364870329410, -1.250000000000000000 ) ) ;
#11650=FACE_OUTER_BOUND ( 'NONE', #6978, .T. ) ;
#11658=VERTEX_POINT ( 'NONE', #10233 ) ;
#11757=ORIENTED_EDGE ( 'NONE', *, *, #12450, .F. ) ;
#11760=VERTEX_POINT ( 'NONE', #7914 ) ;
#11777=DIRECTION ( 'NONE',  ( 0.000000000000000000, 0.000000000000000000, 1.000000000000000000 ) ) ;
#11820=ORIENTED_EDGE ( 'NONE', *, *, #14908, .T. ) ;
#11839=ORIENTED_EDGE ( 'NONE', *, *, #3378, .F. ) ;
#11846=EDGE_LOOP ( 'NONE', ( #14053, #14755 ) ) ;
#11883=CARTESIAN_POINT ( 'NONE',  ( 13.80999999999999872, 0.000000000000000000, 2.000000000000000444 ) ) ;
#11901=AXIS2_PLACEMENT_3D ( 'NONE', #9986, #15848, #7297 ) ;
#11907=( GEOMETRIC_REPRESENTATION_CONTEXT ( 3 ) GLOBAL_UNCERTAINTY_ASSIGNED_CONTEXT ( ( #12376 ) ) GLOBAL_UNIT_ASSIGNED_CONTEXT ( ( #14154, #15381, #11005 ) ) REPRESENTATION_CONTEXT ( 'NONE', 'WORKASPACE' ) );
#11912=CARTESIAN_POINT ( 'NONE',  ( 0.000000000000000000, 0.7216878364870329410, 1.249999999999999778 ) ) ;
#11937=EDGE_CURVE ( 'NONE', #4967, #1717, #12950, .T. ) ;
#11980=ORIENTED_EDGE ( 'NONE', *, *, #7387, .F. ) ;
#11997=AXIS2_PLACEMENT_3D ( 'NONE', #14302, #12627, #14210 ) ;
#12070=ADVANCED_FACE ( 'NONE', ( #12547 ), #10294, .F. ) ;
#12156=CYLINDRICAL_SURFACE ( 'NONE', #6142, 3.799999999999999378 ) ;
#12161=ORIENTED_EDGE ( 'NONE', *, *, #11937, .F. ) ;
#12171=PRODUCT_DEFINITION ( 'UNKNOWN', '', #16965, #6916 ) ;
#12182=EDGE_LOOP ( 'NONE', ( #8203, #15386, #371, #18270 ) ) ;
#12184=DIRECTION ( 'NONE',  ( 1.000000000000000000, 0.000000000000000000, -0.000000000000000000 ) ) ;
#12186=DIRECTION ( 'NONE',  ( 0.000000000000000000, 1.000000000000000000, 0.000000000000000000 ) ) ;
#12197=STYLED_ITEM ( 'NONE', ( #5356 ), #10928 ) ;
#12198=CARTESIAN_POINT ( 'NONE',  ( 0.000000000000000000, -1.443375672974064328, 1.278502688459867223E-18 ) ) ;
#12199=CARTESIAN_POINT ( 'NONE',  ( 2.399999999999999911, 0.000000000000000000, 0.000000000000000000 ) ) ;
#12230=CARTESIAN_POINT ( 'NONE',  ( 0.000000000000000000, 2.449293598294706414E-16, -2.000000000000000000 ) ) ;
#12245=AXIS2_PLACEMENT_3D ( 'NONE', #6795, #9576, #878 ) ;
#12262=EDGE_CURVE ( 'NONE', #4478, #13882, #3000, .T. ) ;
#12319=EDGE_CURVE ( 'NONE', #8355, #9202, #17203, .T. ) ;
#12358=CARTESIAN_POINT ( 'NONE',  ( 0.000000000000000000, 1.443375672974065216, 7.222237291452134449E-31 ) ) ;
#12376=UNCERTAINTY_MEASURE_WITH_UNIT (LENGTH_MEASURE( 1.000000000000000082E-05 ), #14154, 'distance_accuracy_value', 'NONE');
#12405=CARTESIAN_POINT ( 'NONE',  ( 1.300000000000000044, -1.443375672974064328, 2.168404344971008868E-16 ) ) ;
#12441=CARTESIAN_POINT ( 'NONE',  ( 1.300000000000000044, 0.7216878364870329410, 1.249999999999999778 ) ) ;
#12450=EDGE_CURVE ( 'NONE', #13335, #10567, #5027, .T. ) ;
#12454=DIRECTION ( 'NONE',  ( -0.000000000000000000, 0.000000000000000000, -1.000000000000000000 ) ) ;
#12460=CARTESIAN_POINT ( 'NONE',  ( 1.300000000000000044, 0.000000000000000000, 0.000000000000000000 ) ) ;
#12493=FACE_OUTER_BOUND ( 'NONE', #11000, .T. ) ;
#12515=VECTOR ( 'NONE', #12865, 1000.000000000000000 ) ;
#12528=ORIENTED_EDGE ( 'NONE', *, *, #7896, .F. ) ;
#12540=CARTESIAN_POINT ( 'NONE',  ( 1.300000000000000044, 0.7216878364870329410, -1.250000000000000000 ) ) ;
#12547=FACE_OUTER_BOUND ( 'NONE', #17842, .T. ) ;
#12549=CONICAL_SURFACE ( 'NONE', #9601, 1732.050807568857181, 1.047197551196592746 ) ;
#12565=CARTESIAN_POINT ( 'NONE',  ( 1.300000000000000044, -0.7216878364870317197, 1.250000000000000000 ) ) ;
#12586=DIRECTION ( 'NONE',  ( 0.000000000000000000, -0.8660254037844387076, 0.5000000000000001110 ) ) ;
#12627=DIRECTION ( 'NONE',  ( 1.000000000000000000, 0.000000000000000000, -0.000000000000000000 ) ) ;
#12635=CARTESIAN_POINT ( 'NONE',  ( 2.399999999999999911, 0.000000000000000000, 0.000000000000000000 ) ) ;
#12662=AXIS2_PLACEMENT_3D ( 'NONE', #17604, #16008, #3300 ) ;
#12666=UNCERTAINTY_MEASURE_WITH_UNIT (LENGTH_MEASURE( 1.000000000000000082E-05 ), #17600, 'distance_accuracy_value', 'NONE');
#12749=CARTESIAN_POINT ( 'NONE',  ( 2.021687836487040535, 2.168404344971008868E-16, 0.000000000000000000 ) ) ;
#12787=CIRCLE ( 'NONE', #13081, 1.899999999999999689 ) ;
#12852=ADVANCED_FACE ( 'NONE', ( #1781, #6024 ), #17273, .F. ) ;
#12853=ORIENTED_EDGE ( 'NONE', *, *, #1503, .T. ) ;
#12865=DIRECTION ( 'NONE',  ( -1.000000000000000000, -0.000000000000000000, -0.000000000000000000 ) ) ;
#12884=ORIENTED_EDGE ( 'NONE', *, *, #15940, .F. ) ;
#12950=CIRCLE ( 'NONE', #11176, 0.2000000000000000944 ) ;
#12975=ORIENTED_EDGE ( 'NONE', *, *, #17924, .T. ) ;
#13043=DIRECTION ( 'NONE',  ( -1.000000000000000000, -0.000000000000000000, -0.000000000000000000 ) ) ;
#13073=DIRECTION ( 'NONE',  ( -1.000000000000000000, -0.000000000000000000, -0.000000000000000000 ) ) ;
#13081=AXIS2_PLACEMENT_3D ( 'NONE', #15969, #13073, #3261 ) ;
#13099=CARTESIAN_POINT ( 'NONE',  ( 0.000000000000000000, -1.443375672974064328, 1.278502688459867223E-18 ) ) ;
#13107=CIRCLE ( 'NONE', #8657, 3.799999999999999378 ) ;
#13117=EDGE_CURVE ( 'NONE', #15292, #17585, #7016, .T. ) ;
#13132=ORIENTED_EDGE ( 'NONE', *, *, #15462, .T. ) ;
#13137=DIRECTION ( 'NONE',  ( -1.000000000000000000, -0.000000000000000000, -0.000000000000000000 ) ) ;
#13138=CARTESIAN_POINT ( 'NONE',  ( 1.820000000000000062, -3.799999999999999378, -4.653657836759940757E-16 ) ) ;
#13147=LINE ( 'NONE', #3241, #8064 ) ;
#13260=DIRECTION ( 'NONE',  ( 0.000000000000000000, 0.000000000000000000, 1.000000000000000000 ) ) ;
#13265=CARTESIAN_POINT ( 'NONE',  ( 1.300000000000000044, -1.443375672974064328, 1.278502688459867223E-18 ) ) ;
#13335=VERTEX_POINT ( 'NONE', #18276 ) ;
#13350=CARTESIAN_POINT ( 'NONE',  ( -997.9783121635130101, 0.000000000000000000, 0.000000000000000000 ) ) ;
#13371=DIRECTION ( 'NONE',  ( 0.000000000000000000, 0.000000000000000000, 1.000000000000000000 ) ) ;
#13405=AXIS2_PLACEMENT_3D ( 'NONE', #5739, #1573, #11378 ) ;
#13426=DIRECTION ( 'NONE',  ( -0.000000000000000000, -0.5000000000000001110, 0.8660254037844385966 ) ) ;
#13489=PRODUCT_CONTEXT ( 'NONE', #8188, 'mechanical' ) ;
#13518=ADVANCED_FACE ( 'NONE', ( #5819 ), #15942, .T. ) ;
#13557=DIRECTION ( 'NONE',  ( 0.000000000000000000, 0.000000000000000000, 1.000000000000000000 ) ) ;
#13582=MECHANICAL_DESIGN_GEOMETRIC_PRESENTATION_REPRESENTATION('',(#1322),#10883);
#13618=CONICAL_SURFACE ( 'NONE', #15117, 1.610000000000000098, 0.7853981633974469467 ) ;
#13670=CARTESIAN_POINT ( 'NONE',  ( 2.021687836487040535, 0.000000000000000000, 2.168404344971008868E-16 ) ) ;
#13716=ORIENTED_EDGE ( 'NONE', *, *, #6896, .F. ) ;
#13789=EDGE_CURVE ( 'NONE', #16110, #15565, #15531, .T. ) ;
#13813=LINE ( 'NONE', #15126, #9564 ) ;
#13843=CARTESIAN_POINT ( 'NONE',  ( 2.200000000000000178, 4.653657836759941744E-16, -3.799999999999999378 ) ) ;
#13882=VERTEX_POINT ( 'NONE', #13099 ) ;
#13893=ORIENTED_EDGE ( 'NONE', *, *, #15458, .F. ) ;
#13896=DIRECTION ( 'NONE',  ( -1.000000000000000000, -0.000000000000000000, -0.000000000000000000 ) ) ;
#13907=DIRECTION ( 'NONE',  ( -1.000000000000000000, -0.000000000000000000, -0.000000000000000000 ) ) ;
#13925=LINE ( 'NONE', #959, #610 ) ;
#14032=LINE ( 'NONE', #12358, #204 ) ;
#14053=ORIENTED_EDGE ( 'NONE', *, *, #8797, .F. ) ;
#14102=CARTESIAN_POINT ( 'NONE',  ( 1.300000000000000044, -1.443375672974064328, 1.278502688459867223E-18 ) ) ;
#14143=CARTESIAN_POINT ( 'NONE',  ( 0.000000000000000000, 0.7216878364870329410, -1.250000000000000000 ) ) ;
#14154=( LENGTH_UNIT ( ) NAMED_UNIT ( * ) SI_UNIT ( .MILLI., .METRE. ) );
#14210=DIRECTION ( 'NONE',  ( -0.000000000000000000, 0.000000000000000000, -1.000000000000000000 ) ) ;
#14218=DIRECTION ( 'NONE',  ( -1.000000000000000000, -0.000000000000000000, -0.000000000000000000 ) ) ;
#14241=CYLINDRICAL_SURFACE ( 'NONE', #5939, 2.000000000000000000 ) ;
#14248=EDGE_CURVE ( 'NONE', #10194, #278, #10013, .T. ) ;
#14287=DIRECTION ( 'NONE',  ( -0.000000000000000000, 0.000000000000000000, 1.000000000000000000 ) ) ;
#14288=ORIENTED_EDGE ( 'NONE', *, *, #2967, .T. ) ;
#14302=CARTESIAN_POINT ( 'NONE',  ( 1.300000000000000044, -1.443375672974064328, 2.168404344971008868E-16 ) ) ;
#14311=EDGE_CURVE ( 'NONE', #7786, #1402, #8834, .T. ) ;
#14351=DIRECTION ( 'NONE',  ( 0.000000000000000000, 0.8660254037844385966, -0.5000000000000003331 ) ) ;
#14352=PLANE ( 'NONE',  #4727 ) ;
#14382=DIRECTION ( 'NONE',  ( -0.000000000000000000, -0.5000000000000002220, -0.8660254037844384856 ) ) ;
#14386=FACE_OUTER_BOUND ( 'NONE', #2055, .T. ) ;
#14450=CARTESIAN_POINT ( 'NONE',  ( 1.300000000000000044, -1.443375672974064328, 2.168404344971008868E-16 ) ) ;
#14458=ORIENTED_EDGE ( 'NONE', *, *, #14766, .T. ) ;
#14469=VECTOR ( 'NONE', #18134, 1000.000000000000000 ) ;
#14471=VECTOR ( 'NONE', #1801, 1000.000000000000000 ) ;
#14499=VECTOR ( 'NONE', #9440, 1000.000000000000000 ) ;
#14576=CARTESIAN_POINT ( 'NONE',  ( 14.20000000000000107, 0.000000000000000000, 0.000000000000000000 ) ) ;
#14609=CARTESIAN_POINT ( 'NONE',  ( 13.80999999999999872, 0.000000000000000000, 0.000000000000000000 ) ) ;
#14611=EDGE_LOOP ( 'NONE', ( #1621, #13132 ) ) ;
#14619=DIRECTION ( 'NONE',  ( -1.000000000000000000, -0.000000000000000000, -0.000000000000000000 ) ) ;
#14651=DIRECTION ( 'NONE',  ( 0.000000000000000000, 0.000000000000000000, -1.000000000000000000 ) ) ;
#14685=ADVANCED_FACE ( 'NONE', ( #12493 ), #18187, .F. ) ;
#14755=ORIENTED_EDGE ( 'NONE', *, *, #4312, .F. ) ;
#14757=DIRECTION ( 'NONE',  ( -0.000000000000000000, 1.000000000000000000, -0.000000000000000000 ) ) ;
#14766=EDGE_CURVE ( 'NONE', #1083, #11658, #3243, .T. ) ;
#14810=ORIENTED_EDGE ( 'NONE', *, *, #10761, .T. ) ;
#14826=PLANE ( 'NONE',  #7058 ) ;
#14843=CARTESIAN_POINT ( 'NONE',  ( 1.820000000000000062, 0.000000000000000000, 0.000000000000000000 ) ) ;
#14908=EDGE_CURVE ( 'NONE', #1717, #3078, #3533, .T. ) ;
#14913=AXIS2_PLACEMENT_3D ( 'NONE', #10835, #12586, #6751 ) ;
#14948=DIRECTION ( 'NONE',  ( -1.000000000000000000, -0.000000000000000000, -0.000000000000000000 ) ) ;
#14949=FACE_OUTER_BOUND ( 'NONE', #5231, .T. ) ;
#14971=ORIENTED_EDGE ( 'NONE', *, *, #9098, .F. ) ;
#14987=DIRECTION ( 'NONE',  ( 0.000000000000000000, 1.000000000000000000, 1.224646799147353454E-16 ) ) ;
#14996=ADVANCED_FACE ( 'NONE', ( #4972 ), #14826, .T. ) ;
#15025=ORIENTED_EDGE ( 'NONE', *, *, #5346, .F. ) ;
#15026=LINE ( 'NONE', #3787, #14499 ) ;
#15056=ORIENTED_EDGE ( 'NONE', *, *, #2770, .F. ) ;
#15061=ORIENTED_EDGE ( 'NONE', *, *, #15940, .T. ) ;
#15075=FACE_OUTER_BOUND ( 'NONE', #17443, .T. ) ;
#15082=DIRECTION ( 'NONE',  ( -0.5000000000000042188, 0.000000000000000000, 0.8660254037844361541 ) ) ;
#15096=DIRECTION ( 'NONE',  ( -1.000000000000000000, 0.000000000000000000, 0.000000000000000000 ) ) ;
#15105=CIRCLE ( 'NONE', #3254, 2.200000000000000178 ) ;
#15117=AXIS2_PLACEMENT_3D ( 'NONE', #11626, #14619, #1922 ) ;
#15126=CARTESIAN_POINT ( 'NONE',  ( 2.021687836487040535, 2.655529440325959183E-32, -2.168404344971008868E-16 ) ) ;
#15174=DIRECTION ( 'NONE',  ( -1.000000000000000000, -0.000000000000000000, -0.000000000000000000 ) ) ;
#15195=CIRCLE ( 'NONE', #2177, 3.799999999999999378 ) ;
#15213=FACE_OUTER_BOUND ( 'NONE', #16441, .T. ) ;
#15227=ADVANCED_FACE ( 'NONE', ( #14949 ), #2243, .T. ) ;
#15231=EDGE_LOOP ( 'NONE', ( #12975, #10478, #17404, #3235, #17085 ) ) ;
#15285=ORIENTED_EDGE ( 'NONE', *, *, #786, .T. ) ;
#15292=VERTEX_POINT ( 'NONE', #9712 ) ;
#15305=ORIENTED_EDGE ( 'NONE', *, *, #786, .F. ) ;
#15326=CARTESIAN_POINT ( 'NONE',  ( 14.20000000000000107, 0.000000000000000000, 0.000000000000000000 ) ) ;
#15328=ORIENTED_EDGE ( 'NONE', *, *, #4144, .F. ) ;
#15381=( NAMED_UNIT ( * ) PLANE_ANGLE_UNIT ( ) SI_UNIT ( $, .RADIAN. ) );
#15386=ORIENTED_EDGE ( 'NONE', *, *, #7906, .F. ) ;
#15416=AXIS2_PLACEMENT_3D ( 'NONE', #18165, #5435, #3115 ) ;
#15450=CARTESIAN_POINT ( 'NONE',  ( 0.000000000000000000, 0.000000000000000000, 0.000000000000000000 ) ) ;
#15453=EDGE_CURVE ( 'NONE', #1682, #17585, #18068, .T. ) ;
#15458=EDGE_CURVE ( 'NONE', #13335, #8355, #10344, .T. ) ;
#15462=EDGE_CURVE ( 'NONE', #6724, #4967, #15105, .T. ) ;
#15490=VERTEX_POINT ( 'NONE', #13138 ) ;
#15531=LINE ( 'NONE', #8638, #4965 ) ;
#15563=CARTESIAN_POINT ( 'NONE',  ( 1.300000000000000044, 0.000000000000000000, 0.000000000000000000 ) ) ;
#15565=VERTEX_POINT ( 'NONE', #7382 ) ;
#15570=VECTOR ( 'NONE', #11407, 1000.000000000000000 ) ;
#15581=DIRECTION ( 'NONE',  ( 0.000000000000000000, 0.000000000000000000, 1.000000000000000000 ) ) ;
#15590=ORIENTED_EDGE ( 'NONE', *, *, #15458, .T. ) ;
#15606=ADVANCED_FACE ( 'NONE', ( #11650 ), #14352, .F. ) ;
#15607=CYLINDRICAL_SURFACE ( 'NONE', #16612, 3.799999999999999378 ) ;
#15641=SURFACE_STYLE_FILL_AREA ( #4046 ) ;
#15652=FACE_OUTER_BOUND ( 'NONE', #17621, .T. ) ;
#15695=DIRECTION ( 'NONE',  ( 1.000000000000000000, 0.000000000000000000, -0.000000000000000000 ) ) ;
#15729=ORIENTED_EDGE ( 'NONE', *, *, #2770, .T. ) ;
#15759=VERTEX_POINT ( 'NONE', #9330 ) ;
#15765=AXIS2_PLACEMENT_3D ( 'NONE', #6315, #7696, #13260 ) ;
#15777=VECTOR ( 'NONE', #4741, 1000.000000000000000 ) ;
#15780=VECTOR ( 'NONE', #14382, 1000.000000000000114 ) ;
#15848=DIRECTION ( 'NONE',  ( -1.000000000000000000, -0.000000000000000000, -0.000000000000000000 ) ) ;
#15874=ORIENTED_EDGE ( 'NONE', *, *, #11579, .T. ) ;
#15885=ADVANCED_FACE ( 'NONE', ( #16858 ), #16949, .T. ) ;
#15940=EDGE_CURVE ( 'NONE', #3198, #1402, #6793, .T. ) ;
#15942=SPHERICAL_SURFACE ( 'NONE', #4077, 4.324969328314201000 ) ;
#15959=ADVANCED_FACE ( 'NONE', ( #4497 ), #17320, .T. ) ;
#15969=CARTESIAN_POINT ( 'NONE',  ( 8.673617379884035472E-16, 0.000000000000000000, 0.000000000000000000 ) ) ;
#15971=DIRECTION ( 'NONE',  ( 0.000000000000000000, 0.000000000000000000, 1.000000000000000000 ) ) ;
#15986=DIRECTION ( 'NONE',  ( -1.000000000000000000, -0.000000000000000000, -0.000000000000000000 ) ) ;
#16007=CARTESIAN_POINT ( 'NONE',  ( 3.885274725274725949, -4.336808689942017736E-16, 0.000000000000000000 ) ) ;
#16008=DIRECTION ( 'NONE',  ( -1.000000000000000000, -0.000000000000000000, -0.000000000000000000 ) ) ;
#16024=ADVANCED_FACE ( 'NONE', ( #17038 ), #13618, .T. ) ;
#16034=ADVANCED_FACE ( 'NONE', ( #10328 ), #5883, .T. ) ;
#16049=AXIS2_PLACEMENT_3D ( 'NONE', #6357, #10612, #14987 ) ;
#16067=DIRECTION ( 'NONE',  ( -1.000000000000000000, -0.000000000000000000, -0.000000000000000000 ) ) ;
#16084=EDGE_LOOP ( 'NONE', ( #11515, #8579, #6058, #11820 ) ) ;
#16106=CARTESIAN_POINT ( 'NONE',  ( 0.000000000000000000, 0.000000000000000000, 0.000000000000000000 ) ) ;
#16110=VERTEX_POINT ( 'NONE', #2930 ) ;
#16119=ORIENTED_EDGE ( 'NONE', *, *, #17463, .F. ) ;
#16121=DIRECTION ( 'NONE',  ( -0.000000000000000000, 0.000000000000000000, 1.000000000000000000 ) ) ;
#16156=LINE ( 'NONE', #7515, #9822 ) ;
#16208=DIRECTION ( 'NONE',  ( 1.000000000000000000, 0.000000000000000000, -0.000000000000000000 ) ) ;
#16231=EDGE_LOOP ( 'NONE', ( #16818, #16246, #6456 ) ) ;
#16246=ORIENTED_EDGE ( 'NONE', *, *, #17924, .F. ) ;
#16262=VECTOR ( 'NONE', #1118, 1000.000000000000000 ) ;
#16353=CARTESIAN_POINT ( 'NONE',  ( 14.20000000000000107, 0.000000000000000000, 1.610000000000000098 ) ) ;
#16362=CIRCLE ( 'NONE', #15765, 2.000000000000000000 ) ;
#16441=EDGE_LOOP ( 'NONE', ( #481, #15874, #410, #17418, #10766 ) ) ;
#16517=LINE ( 'NONE', #4167, #8935 ) ;
#16554=FACE_OUTER_BOUND ( 'NONE', #169, .T. ) ;
#16556=AXIS2_PLACEMENT_3D ( 'NONE', #17282, #15971, #3264 ) ;
#16612=AXIS2_PLACEMENT_3D ( 'NONE', #2910, #14218, #17764 ) ;
#16643=CARTESIAN_POINT ( 'NONE',  ( -997.9783121635130101, 0.000000000000000000, 0.000000000000000000 ) ) ;
#16678=CARTESIAN_POINT ( 'NONE',  ( 1.300000000000000044, 0.000000000000000000, -1.250000000000000000 ) ) ;
#16692=ORIENTED_EDGE ( 'NONE', *, *, #6615, .T. ) ;
#16727=FACE_OUTER_BOUND ( 'NONE', #11283, .T. ) ;
#16729=EDGE_LOOP ( 'NONE', ( #17943, #17719, #9501, #13716, #10731 ) ) ;
#16730=ORIENTED_EDGE ( 'NONE', *, *, #18156, .F. ) ;
#16759=ORIENTED_EDGE ( 'NONE', *, *, #2155, .T. ) ;
#16763=CARTESIAN_POINT ( 'NONE',  ( 2.199999999999999734, 0.000000000000000000, 0.000000000000000000 ) ) ;
#16788=PLANE ( 'NONE',  #3551 ) ;
#16789=ADVANCED_FACE ( 'NONE', ( #9938 ), #15607, .T. ) ;
#16818=ORIENTED_EDGE ( 'NONE', *, *, #14766, .F. ) ;
#16854=LINE ( 'NONE', #4305, #7663 ) ;
#16858=FACE_OUTER_BOUND ( 'NONE', #15231, .T. ) ;
#16866=ORIENTED_EDGE ( 'NONE', *, *, #4085, .T. ) ;
#16871=EDGE_CURVE ( 'NONE', #6078, #15759, #2100, .T. ) ;
#16935=EDGE_CURVE ( 'NONE', #6078, #15292, #1991, .T. ) ;
#16940=AXIS2_PLACEMENT_3D ( 'NONE', #9024, #13557, #6428 ) ;
#16949=PLANE ( 'NONE',  #8862 ) ;
#16959=( LENGTH_UNIT ( ) NAMED_UNIT ( * ) SI_UNIT ( .MILLI., .METRE. ) );
#16965=PRODUCT_DEFINITION_FORMATION_WITH_SPECIFIED_SOURCE ( 'ANY', '', #3977, .NOT_KNOWN. ) ;
#16973=TOROIDAL_SURFACE ( 'NONE', #13405, 2.200000000000000178, 0.2000000000000000111 ) ;
#16975=ORIENTED_EDGE ( 'NONE', *, *, #1738, .T. ) ;
#16980=CARTESIAN_POINT ( 'NONE',  ( 1.300000000000000044, 1.082531754730548856, -0.6250000000000002220 ) ) ;
#17038=FACE_OUTER_BOUND ( 'NONE', #10440, .T. ) ;
#17047=EDGE_CURVE ( 'NONE', #8977, #1682, #13925, .T. ) ;
#17078=DIRECTION ( 'NONE',  ( -1.000000000000000000, -0.000000000000000000, -0.000000000000000000 ) ) ;
#17084=CARTESIAN_POINT ( 'NONE',  ( 2.199999999999999734, 1.999999999999999112, 0.000000000000000000 ) ) ;
#17085=ORIENTED_EDGE ( 'NONE', *, *, #14248, .F. ) ;
#17129=DIRECTION ( 'NONE',  ( -0.000000000000000000, -1.000000000000000000, 1.502314598737159031E-16 ) ) ;
#17150=ADVANCED_FACE ( 'NONE', ( #16727 ), #9647, .F. ) ;
#17203=LINE ( 'NONE', #8725, #5273 ) ;
#17226=CARTESIAN_POINT ( 'NONE',  ( 1.820000000000000062, 4.653657836759941744E-16, -3.799999999999999378 ) ) ;
#17257=MECHANICAL_DESIGN_GEOMETRIC_PRESENTATION_REPRESENTATION('',(#12197),#11907);
#17273=PLANE ( 'NONE',  #18049 ) ;
#17282=CARTESIAN_POINT ( 'NONE',  ( 3.885274725274725949, -4.336808689942017736E-16, 0.000000000000000000 ) ) ;
#17309=CIRCLE ( 'NONE', #4858, 0.2000000000000000944 ) ;
#17320=SPHERICAL_SURFACE ( 'NONE', #11241, 4.324969328314201000 ) ;
#17344=DIRECTION ( 'NONE',  ( 0.000000000000000000, 0.000000000000000000, 1.000000000000000000 ) ) ;
#17376=CARTESIAN_POINT ( 'NONE',  ( 2.200000000000000178, 0.000000000000000000, 0.000000000000000000 ) ) ;
#17386=EDGE_CURVE ( 'NONE', #11658, #1682, #2708, .T. ) ;
#17389=DIRECTION ( 'NONE',  ( -0.7071067811865484609, 8.659560562354921765E-17, -0.7071067811865465735 ) ) ;
#17404=ORIENTED_EDGE ( 'NONE', *, *, #13789, .T. ) ;
#17418=ORIENTED_EDGE ( 'NONE', *, *, #10397, .F. ) ;
#17433=CARTESIAN_POINT ( 'NONE',  ( 0.000000000000000000, 4.653657836759941744E-16, -3.799999999999999378 ) ) ;
#17439=ORIENTED_EDGE ( 'NONE', *, *, #10397, .T. ) ;
#17443=EDGE_LOOP ( 'NONE', ( #17822, #11839, #10640 ) ) ;
#17463=EDGE_CURVE ( 'NONE', #1083, #16110, #2132, .T. ) ;
#17525=ORIENTED_EDGE ( 'NONE', *, *, #12319, .T. ) ;
#17530=FACE_OUTER_BOUND ( 'NONE', #10483, .T. ) ;
#17585=VERTEX_POINT ( 'NONE', #16678 ) ;
#17588=VECTOR ( 'NONE', #10798, 1000.000000000000000 ) ;
#17595=DIRECTION ( 'NONE',  ( -0.000000000000000000, 1.000000000000000000, 1.224646799147353207E-16 ) ) ;
#17600=( LENGTH_UNIT ( ) NAMED_UNIT ( * ) SI_UNIT ( .MILLI., .METRE. ) );
#17604=CARTESIAN_POINT ( 'NONE',  ( 1.300000000000000044, 0.000000000000000000, 0.000000000000000000 ) ) ;
#17621=EDGE_LOOP ( 'NONE', ( #824, #16759, #6755, #12528, #8678 ) ) ;
#17719=ORIENTED_EDGE ( 'NONE', *, *, #9098, .T. ) ;
#17751=VECTOR ( 'NONE', #7891, 1000.000000000000000 ) ;
#17764=DIRECTION ( 'NONE',  ( 0.000000000000000000, 0.000000000000000000, 1.000000000000000000 ) ) ;
#17793=DIRECTION ( 'NONE',  ( 0.000000000000000000, 0.000000000000000000, 1.000000000000000000 ) ) ;
#17802=ADVANCED_FACE ( 'NONE', ( #5977 ), #14241, .T. ) ;
#17822=ORIENTED_EDGE ( 'NONE', *, *, #17386, .F. ) ;
#17842=EDGE_LOOP ( 'NONE', ( #6668, #11028, #8610, #12161 ) ) ;
#17845=CARTESIAN_POINT ( 'NONE',  ( 0.000000000000000000, 0.000000000000000000, 0.000000000000000000 ) ) ;
#17872=LINE ( 'NONE', #5141, #17588 ) ;
#17884=ORIENTED_EDGE ( 'NONE', *, *, #15453, .F. ) ;
#17917=ORIENTED_EDGE ( 'NONE', *, *, #3203, .T. ) ;
#17921=VERTEX_POINT ( 'NONE', #17226 ) ;
#17924=EDGE_CURVE ( 'NONE', #10194, #1083, #5795, .T. ) ;
#17935=DIRECTION ( 'NONE',  ( 0.000000000000000000, 0.000000000000000000, 1.000000000000000000 ) ) ;
#17939=ORIENTED_EDGE ( 'NONE', *, *, #15453, .T. ) ;
#17943=ORIENTED_EDGE ( 'NONE', *, *, #8797, .T. ) ;
#17974=UNCERTAINTY_MEASURE_WITH_UNIT (LENGTH_MEASURE( 1.000000000000000082E-05 ), #16959, 'distance_accuracy_value', 'NONE');
#17985=DIRECTION ( 'NONE',  ( -0.000000000000000000, -1.000000000000000000, 1.502314598737159031E-16 ) ) ;
#17989=EDGE_LOOP ( 'NONE', ( #14971, #2956, #16975, #2112, #15305 ) ) ;
#18049=AXIS2_PLACEMENT_3D ( 'NONE', #17084, #4546, #14287 ) ;
#18068=CIRCLE ( 'NONE', #2665, 1.250000000000000222 ) ;
#18096=DIRECTION ( 'NONE',  ( 1.000000000000000000, 0.000000000000000000, -0.000000000000000000 ) ) ;
#18134=DIRECTION ( 'NONE',  ( -1.000000000000000000, 0.000000000000000000, 0.000000000000000000 ) ) ;
#18156=EDGE_CURVE ( 'NONE', #15490, #3198, #9508, .T. ) ;
#18165=CARTESIAN_POINT ( 'NONE',  ( 8.673617379884035472E-16, 0.000000000000000000, 0.000000000000000000 ) ) ;
#18166=CARTESIAN_POINT ( 'NONE',  ( 0.000000000000000000, 0.000000000000000000, 2.000000000000000000 ) ) ;
#18187=PLANE ( 'NONE',  #7654 ) ;
#18193=EDGE_LOOP ( 'NONE', ( #11466, #8593, #5168, #546, #3587 ) ) ;
#18243=CARTESIAN_POINT ( 'NONE',  ( 13.80999999999999872, 0.000000000000000000, 0.000000000000000000 ) ) ;
#18260=ORIENTED_EDGE ( 'NONE', *, *, #11239, .F. ) ;
#18270=ORIENTED_EDGE ( 'NONE', *, *, #1449, .F. ) ;
#18276=CARTESIAN_POINT ( 'NONE',  ( 14.20000000000000107, 0.000000000000000000, 1.610000000000000098 ) ) ;
#18324=DIRECTION ( 'NONE',  ( 0.000000000000000000, 0.000000000000000000, 1.000000000000000000 ) ) ;
#18411=COLOUR_RGB('Black',0.12,0.14,0.17);
#18412=FILL_AREA_STYLE_COLOUR('',#18411);
#18413=FILL_AREA_STYLE('',(#18412));
#18414=SURFACE_STYLE_FILL_AREA(#18413);
#18415=SURFACE_SIDE_STYLE('',(#18414));
#18416=SURFACE_STYLE_USAGE(.BOTH.,#18415);
#18417=PRESENTATION_STYLE_ASSIGNMENT((#18416));
ENDSEC;
END-ISO-10303-21;
